ISO-10303-21;
HEADER;
/* Generated by software containing ST-Developer
 * from STEP Tools, Inc. (www.steptools.com) 
 */

FILE_DESCRIPTION(
/* description */ ('PAT-091'),
/* implementation_level */ '2;1');

FILE_NAME(
/* name */ 'Axle distance sleeve 5 mm (5).step',
/* time_stamp */ '2026-10-27T15:34:44-07:00',
/* author */ (''),
/* organization */ (''),
/* preprocessor_version */ 'ST-DEVELOPER v20.2',
/* originating_system */ 'Autodesk Translation Framework v15.17.0.0',
/* authorisation */ '');

FILE_SCHEMA (('AUTOMOTIVE_DESIGN { 1 0 10303 214 3 1 1 }'));
ENDSEC;

DATA;
#10=MECHANICAL_DESIGN_GEOMETRIC_PRESENTATION_REPRESENTATION('',(#1009),#25100);
#789=SHAPE_REPRESENTATION_RELATIONSHIP('SRR','None',#25552,#899);
#899=ADVANCED_BREP_SHAPE_REPRESENTATION('',(#1131),#25022);
#1009=STYLED_ITEM('',(#26191),#1131);
#1131=MANIFOLD_SOLID_BREP('Body1',#13288);
#1424=FACE_BOUND('',#3413,.T.);
#1425=FACE_BOUND('',#3415,.T.);
#1815=PLANE('',#15239);
#1816=PLANE('',#15240);
#2383=FACE_OUTER_BOUND('',#3410,.T.);
#2384=FACE_OUTER_BOUND('',#3411,.T.);
#2385=FACE_OUTER_BOUND('',#3412,.T.);
#2386=FACE_OUTER_BOUND('',#3414,.T.);
#3410=EDGE_LOOP('',(#10296,#10297,#10298,#10299));
#3411=EDGE_LOOP('',(#10300,#10301,#10302,#10303));
#3412=EDGE_LOOP('',(#10304));
#3413=EDGE_LOOP('',(#10305));
#3414=EDGE_LOOP('',(#10306));
#3415=EDGE_LOOP('',(#10307));
#4499=LINE('',#22468,#5239);
#4500=LINE('',#22474,#5240);
#5239=VECTOR('',#18143,0.604999999999997);
#5240=VECTOR('',#18150,0.799999999999997);
#5889=CIRCLE('',#15234,0.604999999999997);
#5890=CIRCLE('',#15235,0.604999999999997);
#5891=CIRCLE('',#15237,0.799999999999997);
#5892=CIRCLE('',#15238,0.799999999999997);
#6822=VERTEX_POINT('',#22465);
#6823=VERTEX_POINT('',#22467);
#6824=VERTEX_POINT('',#22471);
#6825=VERTEX_POINT('',#22473);
#8083=EDGE_CURVE('',#6822,#6822,#5889,.T.);
#8084=EDGE_CURVE('',#6822,#6823,#4499,.T.);
#8085=EDGE_CURVE('',#6823,#6823,#5890,.T.);
#8086=EDGE_CURVE('',#6824,#6824,#5891,.T.);
#8087=EDGE_CURVE('',#6824,#6825,#4500,.T.);
#8088=EDGE_CURVE('',#6825,#6825,#5892,.T.);
#10296=ORIENTED_EDGE('',*,*,#8083,.F.);
#10297=ORIENTED_EDGE('',*,*,#8084,.T.);
#10298=ORIENTED_EDGE('',*,*,#8085,.T.);
#10299=ORIENTED_EDGE('',*,*,#8084,.F.);
#10300=ORIENTED_EDGE('',*,*,#8086,.F.);
#10301=ORIENTED_EDGE('',*,*,#8087,.T.);
#10302=ORIENTED_EDGE('',*,*,#8088,.T.);
#10303=ORIENTED_EDGE('',*,*,#8087,.F.);
#10304=ORIENTED_EDGE('',*,*,#8086,.T.);
#10305=ORIENTED_EDGE('',*,*,#8083,.T.);
#10306=ORIENTED_EDGE('',*,*,#8088,.F.);
#10307=ORIENTED_EDGE('',*,*,#8085,.F.);
#12212=CYLINDRICAL_SURFACE('',#15233,0.604999999999997);
#12213=CYLINDRICAL_SURFACE('',#15236,0.799999999999997);
#12750=ADVANCED_FACE('',(#2383),#12212,.F.);
#12751=ADVANCED_FACE('',(#2384),#12213,.T.);
#12752=ADVANCED_FACE('',(#2385,#1424),#1815,.T.);
#12753=ADVANCED_FACE('',(#2386,#1425),#1816,.F.);
#13288=CLOSED_SHELL('',(#12750,#12751,#12752,#12753));
#15232=AXIS2_PLACEMENT_3D('',#22463,#18137,#18138);
#15233=AXIS2_PLACEMENT_3D('',#22464,#18139,#18140);
#15234=AXIS2_PLACEMENT_3D('',#22466,#18141,#18142);
#15235=AXIS2_PLACEMENT_3D('',#22469,#18144,#18145);
#15236=AXIS2_PLACEMENT_3D('',#22470,#18146,#18147);
#15237=AXIS2_PLACEMENT_3D('',#22472,#18148,#18149);
#15238=AXIS2_PLACEMENT_3D('',#22475,#18151,#18152);
#15239=AXIS2_PLACEMENT_3D('',#22476,#18153,#18154);
#15240=AXIS2_PLACEMENT_3D('',#22477,#18155,#18156);
#18137=DIRECTION('axis',(0.,0.,1.));
#18138=DIRECTION('refdir',(1.,0.,0.));
#18139=DIRECTION('center_axis',(0.,1.,0.));
#18140=DIRECTION('ref_axis',(1.,0.,0.));
#18141=DIRECTION('center_axis',(0.,-1.,0.));
#18142=DIRECTION('ref_axis',(1.,0.,0.));
#18143=DIRECTION('',(0.,-1.,0.));
#18144=DIRECTION('center_axis',(0.,-1.,0.));
#18145=DIRECTION('ref_axis',(1.,0.,0.));
#18146=DIRECTION('center_axis',(0.,1.,0.));
#18147=DIRECTION('ref_axis',(1.,0.,0.));
#18148=DIRECTION('center_axis',(0.,1.,0.));
#18149=DIRECTION('ref_axis',(1.,0.,0.));
#18150=DIRECTION('',(0.,-1.,0.));
#18151=DIRECTION('center_axis',(0.,1.,0.));
#18152=DIRECTION('ref_axis',(1.,0.,0.));
#18153=DIRECTION('center_axis',(0.,1.,0.));
#18154=DIRECTION('ref_axis',(1.,0.,0.));
#18155=DIRECTION('center_axis',(0.,1.,0.));
#18156=DIRECTION('ref_axis',(1.,0.,0.));
#22463=CARTESIAN_POINT('',(0.,0.,0.));
#22464=CARTESIAN_POINT('Origin',(38.7298334620742,-6.,3.));
#22465=CARTESIAN_POINT('',(38.1248334620742,-5.5,3.));
#22466=CARTESIAN_POINT('Origin',(38.7298334620742,-5.5,3.));
#22467=CARTESIAN_POINT('',(38.1248334620742,-6.,3.));
#22468=CARTESIAN_POINT('',(38.1248334620742,-6.,3.));
#22469=CARTESIAN_POINT('Origin',(38.7298334620742,-6.,3.));
#22470=CARTESIAN_POINT('Origin',(38.7298334620742,-6.,3.));
#22471=CARTESIAN_POINT('',(37.9298334620742,-5.5,3.));
#22472=CARTESIAN_POINT('Origin',(38.7298334620742,-5.5,3.));
#22473=CARTESIAN_POINT('',(37.9298334620742,-6.,3.));
#22474=CARTESIAN_POINT('',(37.9298334620742,-6.,3.));
#22475=CARTESIAN_POINT('Origin',(38.7298334620742,-6.,3.));
#22476=CARTESIAN_POINT('Origin',(38.7298334620742,-5.5,3.));
#22477=CARTESIAN_POINT('Origin',(38.7298334620742,-6.,3.));
#24901=UNCERTAINTY_MEASURE_WITH_UNIT(LENGTH_MEASURE(0.001),#25101,
'DISTANCE_ACCURACY_VALUE',
'Maximum model space distance between geometric entities at asserted c
onnectivities');
#24979=UNCERTAINTY_MEASURE_WITH_UNIT(LENGTH_MEASURE(0.001),#25101,
'DISTANCE_ACCURACY_VALUE',
'Maximum model space distance between geometric entities at asserted c
onnectivities');
#25022=(
GEOMETRIC_REPRESENTATION_CONTEXT(3)
GLOBAL_UNCERTAINTY_ASSIGNED_CONTEXT((#24901))
GLOBAL_UNIT_ASSIGNED_CONTEXT((#25101,#25103,#25104))
REPRESENTATION_CONTEXT('','3D')
);
#25100=(
GEOMETRIC_REPRESENTATION_CONTEXT(3)
GLOBAL_UNCERTAINTY_ASSIGNED_CONTEXT((#24979))
GLOBAL_UNIT_ASSIGNED_CONTEXT((#25101,#25103,#25104))
REPRESENTATION_CONTEXT('','3D')
);
#25101=(
LENGTH_UNIT()
NAMED_UNIT(*)
SI_UNIT(.CENTI.,.METRE.)
);
#25103=(
NAMED_UNIT(*)
PLANE_ANGLE_UNIT()
SI_UNIT($,.RADIAN.)
);
#25104=(
NAMED_UNIT(*)
SI_UNIT($,.STERADIAN.)
SOLID_ANGLE_UNIT()
);
#25147=SHAPE_DEFINITION_REPRESENTATION(#25267,#25552);
#25267=PRODUCT_DEFINITION_SHAPE('',$,#25673);
#25552=SHAPE_REPRESENTATION('',(#15232),#25022);
#25630=PRODUCT_DEFINITION_CONTEXT('part definition',#25992,'design');
#25673=PRODUCT_DEFINITION('Axle distance sleeve 5 mm (5)',
'Axle distance sleeve 5 mm (5)',#25793,#25630);
#25793=PRODUCT_DEFINITION_FORMATION('',$,#26036);
#25992=APPLICATION_CONTEXT(
'Core Data for Automotive Mechanical Design Process');
#25993=PRODUCT_CONTEXT('part definition',#25992,'mechanical');
#26036=PRODUCT('Axle distance sleeve 5 mm (5)',
'Axle distance sleeve 5 mm (5)','Axle distance sleeve 5 mm (5)',(#25993));
#26185=COLOUR_RGB('Grey',0.48,0.52,0.57);
#26186=FILL_AREA_STYLE_COLOUR('',#26185);
#26187=FILL_AREA_STYLE('',(#26186));
#26188=SURFACE_STYLE_FILL_AREA(#26187);
#26189=SURFACE_SIDE_STYLE('',(#26188));
#26190=SURFACE_STYLE_USAGE(.BOTH.,#26189);
#26191=PRESENTATION_STYLE_ASSIGNMENT((#26190));
ENDSEC;
END-ISO-10303-21;
